ISO-10303-21;
HEADER;
FILE_DESCRIPTION (('STEP AP214'),
    '1' );
FILE_NAME ('slotted cheese head screw_iso_ISO 1207 - M3 x 5 - 5N.step',
    '2026-10-04T10:31:01',
    ( '' ),
    ( '' ),
    'SwSTEP 2.0',
    'SolidWorks 2026',
    '' );
FILE_SCHEMA (( 'AUTOMOTIVE_DESIGN' ));
ENDSEC;

DATA;
#70=EDGE_CURVE ( 'NONE', #13541, #6298, #6755, .T. ) ;
#82=ORIENTED_EDGE ( 'NONE', *, *, #7980, .T. ) ;
#170=DIRECTION ( 'NONE',  ( -1.000000000000000000, 3.326610055774637112E-18, 1.062480551894331163E-17 ) ) ;
#193=B_SPLINE_CURVE_WITH_KNOTS ( 'NONE', 3,
 ( #6450, #7867, #11284, #4121, #12707, #459, #1650 ),
 .UNSPECIFIED., .F., .F.,
 ( 4, 3, 4 ),
 ( 0.004471049636504374758, 0.004805482912052319762, 0.005232732616948215093 ),
 .UNSPECIFIED. ) ;
#267=EDGE_CURVE ( 'NONE', #4415, #8748, #895, .T. ) ;
#310=CARTESIAN_POINT ( 'NONE',  ( 0.03370811714257901381, -0.3999999999999941380, -2.527096502121718657 ) ) ;
#314=CARTESIAN_POINT ( 'NONE',  ( 0.8499999999999896527, -0.3999999999999906408, -2.750000000000010658 ) ) ;
#321=CIRCLE ( 'NONE', #9221, 2.649388036945190095 ) ;
#342=DIRECTION ( 'NONE',  ( 0.000000000000000000, -2.775557561562887900E-16, 1.000000000000000000 ) ) ;
#384=CARTESIAN_POINT ( 'NONE',  ( 0.06404007393981200891, -0.3999999999999941380, -2.546123937053038855 ) ) ;
#387=CARTESIAN_POINT ( 'NONE',  ( 0.2023276174656383763, -0.3999999999999898637, 2.561683098399103020 ) ) ;
#441=CARTESIAN_POINT ( 'NONE',  ( 0.000000000000000000, -0.3999999999999958589, -2.450963827680254337 ) ) ;
#459=CARTESIAN_POINT ( 'NONE',  ( 0.7081379353438700397, 0.4000000000000047962, -2.606463079733443600 ) ) ;
#499=CYLINDRICAL_SURFACE ( 'NONE', #8108, 1.500000000000001776 ) ;
#521=PRESENTATION_STYLE_ASSIGNMENT (( #13881 ) ) ;
#526=PRODUCT_DEFINITION_CONTEXT ( 'detailed design', #5064, 'design' ) ;
#540=CARTESIAN_POINT ( 'NONE',  ( 0.009591240409140278089, -0.3999999999999975797, -2.494254166949156026 ) ) ;
#607=FACE_OUTER_BOUND ( 'NONE', #2207, .T. ) ;
#609=ORIENTED_EDGE ( 'NONE', *, *, #9405, .F. ) ;
#614=PRESENTATION_STYLE_ASSIGNMENT (( #15259 ) ) ;
#696=CARTESIAN_POINT ( 'NONE',  ( 0.01012247443264182103, 0.4000000000000027978, 2.496776319709509639 ) ) ;
#723=ORIENTED_EDGE ( 'NONE', *, *, #10280, .F. ) ;
#738=COLOUR_RGB ( '', 0.66274510, 0.83137255, 0.94901961) ;
#744=ORIENTED_EDGE ( 'NONE', *, *, #70, .F. ) ;
#767=CARTESIAN_POINT ( 'NONE',  ( 2.000000000000001776, 1.500000000000008216, -8.673617379884158732E-16 ) ) ;
#781=CARTESIAN_POINT ( 'NONE',  ( 0.05741246108494903189, 0.4000000000000045186, 2.543273608808054753 ) ) ;
#783=ORIENTED_EDGE ( 'NONE', *, *, #12609, .T. ) ;
#835=CARTESIAN_POINT ( 'NONE',  ( -1.257347874116830337E-14, 0.4000000000000047962, -2.458352573764722937 ) ) ;
#876=ORIENTED_EDGE ( 'NONE', *, *, #267, .F. ) ;
#895=CIRCLE ( 'NONE', #8543, 2.483389555546411831 ) ;
#899=CARTESIAN_POINT ( 'NONE',  ( 0.8499999999999896527, 0.000000000000000000, 0.000000000000000000 ) ) ;
#909=DIRECTION ( 'NONE',  ( 0.000000000000000000, -2.775557561562887900E-16, 1.000000000000000000 ) ) ;
#910=CARTESIAN_POINT ( 'NONE',  ( 0.01536757896558604841, 0.4000000000000027978, -2.504920264071737179 ) ) ;
#980=ORIENTED_EDGE ( 'NONE', *, *, #10036, .F. ) ;
#1004=VERTEX_POINT ( 'NONE', #11365 ) ;
#1006=CARTESIAN_POINT ( 'NONE',  ( 0.3133709289735966963, 0.4000000000000062395, 2.571515392583430426 ) ) ;
#1035=EDGE_CURVE ( 'NONE', #3171, #11235, #11462, .T. ) ;
#1059=DIRECTION ( 'NONE',  ( 1.000000000000000000, -3.326610055774637112E-18, -1.062480551894331163E-17 ) ) ;
#1070=CARTESIAN_POINT ( 'NONE',  ( 0.8499999999999896527, -4.137240605787344953E-16, 2.649388036945189207 ) ) ;
#1086=CARTESIAN_POINT ( 'NONE',  ( 0.002340087947992566201, -0.3999999999999958589, 2.475597248086677915 ) ) ;
#1139=EDGE_CURVE ( 'NONE', #13047, #4415, #4251, .T. ) ;
#1148=CARTESIAN_POINT ( 'NONE',  ( 0.8499999999999896527, -0.3999999999999906408, -2.750000000000010658 ) ) ;
#1240=CARTESIAN_POINT ( 'NONE',  ( 0.06960442597363748762, -0.3999999999999923617, 2.548071207443342701 ) ) ;
#1258=CARTESIAN_POINT ( 'NONE',  ( 0.000000000000000000, 0.000000000000000000, 0.000000000000000000 ) ) ;
#1319=LINE ( 'NONE', #1789, #9211 ) ;
#1398=DIRECTION ( 'NONE',  ( 0.000000000000000000, -2.775557561562888393E-16, 1.000000000000000000 ) ) ;
#1412=DIRECTION ( 'NONE',  ( 0.9961946980917455452, 2.087662678150794344E-17, -0.08715574274765844343 ) ) ;
#1440=CARTESIAN_POINT ( 'NONE',  ( 0.000000000000000000, 0.4000000000000097367, 2.450963827680236129 ) ) ;
#1498=AXIS2_PLACEMENT_3D ( 'NONE', #11832, #4612, #13110 ) ;
#1532=VERTEX_POINT ( 'NONE', #14606 ) ;
#1561=CARTESIAN_POINT ( 'NONE',  ( 2.000000000000001776, 0.000000000000000000, 0.000000000000000000 ) ) ;
#1577=DIRECTION ( 'NONE',  ( -1.062480551894329776E-17, -2.775557561562888393E-16, 1.000000000000000000 ) ) ;
#1582=ORIENTED_EDGE ( 'NONE', *, *, #1139, .F. ) ;
#1650=CARTESIAN_POINT ( 'NONE',  ( 0.8499999999999896527, 0.4000000000000097367, -2.619018321873355593 ) ) ;
#1651=DIRECTION ( 'NONE',  ( 1.000000000000000000, 0.000000000000000000, 0.000000000000000000 ) ) ;
#1657=CARTESIAN_POINT ( 'NONE',  ( 0.7081379353438682633, -0.3999999999999898637, 2.606463079733445376 ) ) ;
#1728=SURFACE_STYLE_FILL_AREA ( #15106 ) ;
#1745=ORIENTED_EDGE ( 'NONE', *, *, #3115, .T. ) ;
#1789=CARTESIAN_POINT ( 'NONE',  ( 0.000000000000000000, -0.3999999999999906408, -2.750000000000010658 ) ) ;
#1835=ORIENTED_EDGE ( 'NONE', *, *, #12602, .T. ) ;
#1869=CARTESIAN_POINT ( 'NONE',  ( 0.02899383802118515874, 0.4000000000000097367, -2.522283165497673618 ) ) ;
#1879=CARTESIAN_POINT ( 'NONE',  ( 0.5662760513513176441, 0.4000000000000062395, 2.593905796087985216 ) ) ;
#1890=CARTESIAN_POINT ( 'NONE',  ( 0.04799661009841083015, 0.4000000000000045186, 2.537470117151901405 ) ) ;
#1894=EDGE_CURVE ( 'NONE', #1004, #3420, #14147, .T. ) ;
#1968=CARTESIAN_POINT ( 'NONE',  ( 1.511918676366796888E-05, 0.4000000000000080158, 2.452725668627568023 ) ) ;
#2010=ADVANCED_FACE ( 'NONE', ( #9631 ), #10356, .T. ) ;
#2024=CARTESIAN_POINT ( 'NONE',  ( 0.009304900478233046543, 0.4000000000000027978, -2.495165599816074664 ) ) ;
#2033=CARTESIAN_POINT ( 'NONE',  ( 7.000000000000006217, 1.500000000000008216, -8.673617379884158732E-16 ) ) ;
#2038=ORIENTED_EDGE ( 'NONE', *, *, #13999, .F. ) ;
#2065=EDGE_CURVE ( 'NONE', #3287, #3420, #10896, .T. ) ;
#2068=ORIENTED_EDGE ( 'NONE', *, *, #12918, .F. ) ;
#2152=AXIS2_PLACEMENT_3D ( 'NONE', #15148, #11554, #12744 ) ;
#2165=VERTEX_POINT ( 'NONE', #11281 ) ;
#2178=CARTESIAN_POINT ( 'NONE',  ( 0.03680535197730239877, 0.4000000000000097367, -2.530258816757608997 ) ) ;
#2192=ORIENTED_EDGE ( 'NONE', *, *, #3958, .F. ) ;
#2207=EDGE_LOOP ( 'NONE', ( #744, #15528 ) ) ;
#2226=ORIENTED_EDGE ( 'NONE', *, *, #8279, .F. ) ;
#2237=DIRECTION ( 'NONE',  ( -1.000000000000000000, 3.326610055774637112E-18, 1.062480551894331163E-17 ) ) ;
#2273=CARTESIAN_POINT ( 'NONE',  ( 0.01099607048649087204, -0.3999999999999993006, 2.497144250189434533 ) ) ;
#2325=CARTESIAN_POINT ( 'NONE',  ( 0.09128442572522987852, 0.000000000000000000, 0.000000000000000000 ) ) ;
#2355=CARTESIAN_POINT ( 'NONE',  ( 0.03964714319856429969, -0.3999999999999923617, 2.532520041490997187 ) ) ;
#2411=ORIENTED_EDGE ( 'NONE', *, *, #8456, .T. ) ;
#2451=PRODUCT ( 'slotted cheese head screw_iso_ISO 1207 - M3 x 5 - 5N', 'slotted cheese head screw_iso_ISO 1207 - M3 x 5 - 5N', '', ( #3281 ) ) ;
#2704=CARTESIAN_POINT ( 'NONE',  ( 0.3133709289734071812, -0.3999999999999975797, 2.571515392583413107 ) ) ;
#2714=ORIENTED_EDGE ( 'NONE', *, *, #11323, .F. ) ;
#2732=EDGE_LOOP ( 'NONE', ( #2226, #7584, #10910, #13634 ) ) ;
#2733=PRODUCT_DEFINITION_FORMATION_WITH_SPECIFIED_SOURCE ( 'ANY', '', #2451, .NOT_KNOWN. ) ;
#2759=SURFACE_STYLE_FILL_AREA ( #10313 ) ;
#2776=STYLED_ITEM ( 'NONE', ( #614 ), #15721 ) ;
#2779=CARTESIAN_POINT ( 'NONE',  ( 0.004787046309016708585, -0.3999999999999975797, -2.483960639863540099 ) ) ;
#2797=DIRECTION ( 'NONE',  ( 0.000000000000000000, -2.775557561562887900E-16, 1.000000000000000000 ) ) ;
#2841=( LENGTH_UNIT ( ) NAMED_UNIT ( * ) SI_UNIT ( .MILLI., .METRE. ) );
#2857=CARTESIAN_POINT ( 'NONE',  ( 0.0001777891039407533040, -0.3999999999999906408, -2.457936153810343693 ) ) ;
#2894=CARTESIAN_POINT ( 'NONE',  ( 0.2023276174864365173, -0.3999999999999906408, -2.561683098400944658 ) ) ;
#2898=FACE_OUTER_BOUND ( 'NONE', #13292, .T. ) ;
#2916=EDGE_CURVE ( 'NONE', #4415, #8748, #15279, .T. ) ;
#2942=DIRECTION ( 'NONE',  ( -1.062480551894329468E-17, -3.608224830031754812E-16, 1.000000000000000000 ) ) ;
#2956=CARTESIAN_POINT ( 'NONE',  ( 2.000000000000001776, -4.331536797758218293E-16, 2.750000000000002665 ) ) ;
#2995=CARTESIAN_POINT ( 'NONE',  ( 0.8499999999999896527, -0.3999999999999958589, 2.619018321873339161 ) ) ;
#2999=CARTESIAN_POINT ( 'NONE',  ( 0.09128442572522987852, 0.4000000000000062395, -2.551849451881606168 ) ) ;
#3081=DIRECTION ( 'NONE',  ( -1.000000000000000000, 3.326610055774637112E-18, 1.062480551894331163E-17 ) ) ;
#3103=AXIS2_PLACEMENT_3D ( 'NONE', #6546, #170, #2797 ) ;
#3115=EDGE_CURVE ( 'NONE', #9879, #2165, #193, .T. ) ;
#3149=VECTOR ( 'NONE', #2942, 1000.000000000000000 ) ;
#3150=CARTESIAN_POINT ( 'NONE',  ( 0.05609725182637026464, 0.4000000000000045186, -2.541957560783562720 ) ) ;
#3171=VERTEX_POINT ( 'NONE', #15257 ) ;
#3173=DIRECTION ( 'NONE',  ( 1.062480551894329776E-17, 2.775557561562888393E-16, -1.000000000000000000 ) ) ;
#3211=DIRECTION ( 'NONE',  ( 0.000000000000000000, -2.775557561562888393E-16, 1.000000000000000000 ) ) ;
#3254=CIRCLE ( 'NONE', #13929, 2.649388036945190095 ) ;
#3281=PRODUCT_CONTEXT ( 'NONE', #15331, 'mechanical' ) ;
#3287=VERTEX_POINT ( 'NONE', #1070 ) ;
#3292=( GEOMETRIC_REPRESENTATION_CONTEXT ( 3 ) GLOBAL_UNCERTAINTY_ASSIGNED_CONTEXT ( ( #9673 ) ) GLOBAL_UNIT_ASSIGNED_CONTEXT ( ( #2841, #8898, #7687 ) ) REPRESENTATION_CONTEXT ( 'NONE', 'WORKASPACE' ) );
#3365=DIRECTION ( 'NONE',  ( 0.000000000000000000, 9.159339953157539881E-15, -1.000000000000000000 ) ) ;
#3368=LINE ( 'NONE', #10774, #9634 ) ;
#3382=PLANE ( 'NONE',  #7329 ) ;
#3420=VERTEX_POINT ( 'NONE', #2956 ) ;
#3489=VECTOR ( 'NONE', #7082, 1000.000000000000000 ) ;
#3498=AXIS2_PLACEMENT_3D ( 'NONE', #2033, #6830, #11666 ) ;
#3509=EDGE_LOOP ( 'NONE', ( #12911, #2411, #5686, #10267, #783, #4693 ) ) ;
#3634=CARTESIAN_POINT ( 'NONE',  ( 0.8499999999999896527, 0.4000000000000062395, 2.749999999999994227 ) ) ;
#3698=FACE_OUTER_BOUND ( 'NONE', #3509, .T. ) ;
#3739=VECTOR ( 'NONE', #8200, 1000.000000000000000 ) ;
#3805=DIRECTION ( 'NONE',  ( 1.000000000000000000, -3.326610055774637112E-18, -1.062480551894331163E-17 ) ) ;
#3817=EDGE_LOOP ( 'NONE', ( #8785, #2038 ) ) ;
#3958=EDGE_CURVE ( 'NONE', #15527, #7039, #4519, .T. ) ;
#3962=CARTESIAN_POINT ( 'NONE',  ( 0.000000000000000000, 0.000000000000000000, 0.000000000000000000 ) ) ;
#4045=CARTESIAN_POINT ( 'NONE',  ( 0.02104286312898811379, -0.3999999999999941380, -2.514165122916821371 ) ) ;
#4076=DIRECTION ( 'NONE',  ( -1.000000000000000000, 3.326610055774637112E-18, 1.062480551894331163E-17 ) ) ;
#4083=CARTESIAN_POINT ( 'NONE',  ( 0.8499999999999896527, -0.3999999999999941380, -2.619018321873356037 ) ) ;
#4088=ADVANCED_FACE ( 'NONE', ( #5171 ), #13666, .T. ) ;
#4107=( NAMED_UNIT ( * ) PLANE_ANGLE_UNIT ( ) SI_UNIT ( $, .RADIAN. ) );
#4121=CARTESIAN_POINT ( 'NONE',  ( 0.4244143561419055910, 0.4000000000000062395, -2.581346380257607986 ) ) ;
#4122=FILL_AREA_STYLE_COLOUR ( '', #738 ) ;
#4174=DIRECTION ( 'NONE',  ( -1.000000000000000000, 3.326610055774637112E-18, 1.062480551894331163E-17 ) ) ;
#4204=( LENGTH_UNIT ( ) NAMED_UNIT ( * ) SI_UNIT ( .MILLI., .METRE. ) );
#4251=B_SPLINE_CURVE_WITH_KNOTS ( 'NONE', 3,
 ( #15112, #6922, #10567, #4523, #5570, #781, #1890, #8110, #6765, #13987, #7873, #696, #10416, #14061, #8026, #1968, #6845, #9080, #5643 ),
 .UNSPECIFIED., .F., .F.,
 ( 4, 3, 3, 3, 3, 3, 4 ),
 ( 0.0003917759849713744504, 0.0004043855146501730080, 0.0004375639695040863583, 0.0004708920258237459097, 0.0005045670765489163306, 0.0005386560839275773317, 0.0005403960448094325937 ),
 .UNSPECIFIED. ) ;
#4266=CARTESIAN_POINT ( 'NONE',  ( 0.06610679800811947171, 0.4000000000000045186, -2.546908780914493242 ) ) ;
#4273=PLANE ( 'NONE',  #13917 ) ;
#4393=VECTOR ( 'NONE', #2237, 1000.000000000000000 ) ;
#4415=VERTEX_POINT ( 'NONE', #1440 ) ;
#4519=B_SPLINE_CURVE_WITH_KNOTS ( 'NONE', 3,
 ( #11287, #14872, #14953, #6455, #384, #5254, #13824, #15031, #310, #7706, #4045, #9075, #540, #2779, #10178, #12631, #2857, #10024, #12710 ),
 .UNSPECIFIED., .F., .F.,
 ( 4, 3, 3, 3, 3, 3, 4 ),
 ( 0.0005593596330526128761, 0.0005760969326736956617, 0.0006092698741508170094, 0.0006292927786811800201, 0.0006633821546468323532, 0.0006974534310236257589, 0.0007078329331167276936 ),
 .UNSPECIFIED. ) ;
#4523=CARTESIAN_POINT ( 'NONE',  ( 0.07875310241295396807, 0.4000000000000045186, 2.549923512967463335 ) ) ;
#4530=AXIS2_PLACEMENT_3D ( 'NONE', #3962, #12476, #1577 ) ;
#4573=( GEOMETRIC_REPRESENTATION_CONTEXT ( 3 ) GLOBAL_UNCERTAINTY_ASSIGNED_CONTEXT ( ( #12199 ) ) GLOBAL_UNIT_ASSIGNED_CONTEXT ( ( #12535, #4107, #11344 ) ) REPRESENTATION_CONTEXT ( 'NONE', 'WORKASPACE' ) );
#4576=ORIENTED_EDGE ( 'NONE', *, *, #13999, .T. ) ;
#4596=SHAPE_REPRESENTATION ( 'slotted cheese head screw_iso_ISO 1207 - M3 x 5 - 5N', ( #14201 ), #3292 ) ;
#4608=CARTESIAN_POINT ( 'NONE',  ( 0.09128442572522987852, 0.000000000000000000, 0.000000000000000000 ) ) ;
#4612=DIRECTION ( 'NONE',  ( -1.000000000000000000, 3.326610055774643275E-18, -1.062480551894329622E-17 ) ) ;
#4673=CARTESIAN_POINT ( 'NONE',  ( 0.09128442572411965550, -0.3999999999999975797, 2.551849451881568420 ) ) ;
#4689=ORIENTED_EDGE ( 'NONE', *, *, #12602, .F. ) ;
#4693=ORIENTED_EDGE ( 'NONE', *, *, #9405, .T. ) ;
#4707=CIRCLE ( 'NONE', #13582, 2.483389555546411831 ) ;
#4810=ORIENTED_EDGE ( 'NONE', *, *, #11323, .T. ) ;
#4818=( GEOMETRIC_REPRESENTATION_CONTEXT ( 3 ) GLOBAL_UNCERTAINTY_ASSIGNED_CONTEXT ( ( #14595 ) ) GLOBAL_UNIT_ASSIGNED_CONTEXT ( ( #4204, #10330, #8995 ) ) REPRESENTATION_CONTEXT ( 'NONE', 'WORKASPACE' ) );
#4833=CARTESIAN_POINT ( 'NONE',  ( -1.354742131312345542E-14, -0.3999999999999899192, 2.455386912753366957 ) ) ;
#4869=EDGE_LOOP ( 'NONE', ( #10499, #7138 ) ) ;
#4870=ORIENTED_EDGE ( 'NONE', *, *, #2916, .T. ) ;
#4880=DIRECTION ( 'NONE',  ( 0.000000000000000000, 2.775557561562887900E-16, -1.000000000000000000 ) ) ;
#4911=CARTESIAN_POINT ( 'NONE',  ( 2.000000000000001776, 5.005650134388747156E-16, -1.500000000000000000 ) ) ;
#4927=ORIENTED_EDGE ( 'NONE', *, *, #15329, .F. ) ;
#5064=APPLICATION_CONTEXT ( 'automotive_design' ) ;
#5090=CARTESIAN_POINT ( 'NONE',  ( 2.735911510694367108E-17, 7.147123651097129995E-16, -2.575022672948154234 ) ) ;
#5128=ADVANCED_FACE ( 'NONE', ( #7003 ), #8276, .T. ) ;
#5171=FACE_OUTER_BOUND ( 'NONE', #4869, .T. ) ;
#5214=B_SPLINE_CURVE_WITH_KNOTS ( 'NONE', 3,
 ( #7300, #4833, #8420, #8504, #1086, #11896, #2273, #13256, #9689, #14447, #2355, #12140, #7224, #1240, #14359, #4673 ),
 .UNSPECIFIED., .F., .F.,
 ( 4, 3, 3, 3, 3, 4 ),
 ( 8.915077171950578868E-05, 0.0001023483930351222872, 0.0001368170539646130666, 0.0001711500869964550833, 0.0002051216925220995921, 0.0002377972641794323314 ),
 .UNSPECIFIED. ) ;
#5234=FILL_AREA_STYLE_COLOUR ( '', #11177 ) ;
#5254=CARTESIAN_POINT ( 'NONE',  ( 0.05368748911329641882, -0.3999999999999923617, -2.541415605245799902 ) ) ;
#5257=CARTESIAN_POINT ( 'NONE',  ( 0.4244143561419055910, -0.3999999999999975797, 2.581346380257588891 ) ) ;
#5263=FACE_OUTER_BOUND ( 'NONE', #11388, .T. ) ;
#5321=CARTESIAN_POINT ( 'NONE',  ( 0.8499999999999896527, 0.000000000000000000, 0.000000000000000000 ) ) ;
#5342=ORIENTED_EDGE ( 'NONE', *, *, #1035, .F. ) ;
#5443=AXIS2_PLACEMENT_3D ( 'NONE', #6766, #11683, #5571 ) ;
#5465=EDGE_CURVE ( 'NONE', #14081, #13047, #10371, .T. ) ;
#5479=FACE_BOUND ( 'NONE', #6730, .T. ) ;
#5547=CARTESIAN_POINT ( 'NONE',  ( 0.0008067760839495599114, 0.4000000000000062395, -2.465784186028391112 ) ) ;
#5565=LINE ( 'NONE', #3634, #8768 ) ;
#5570=CARTESIAN_POINT ( 'NONE',  ( 0.06795095462586417390, 0.4000000000000045186, 2.547546041960362828 ) ) ;
#5571=DIRECTION ( 'NONE',  ( 1.062480551894331009E-17, -2.775557561562888393E-16, 1.000000000000000000 ) ) ;
#5586=FACE_OUTER_BOUND ( 'NONE', #9560, .T. ) ;
#5643=CARTESIAN_POINT ( 'NONE',  ( 0.000000000000000000, 0.4000000000000097367, 2.450963827680236129 ) ) ;
#5653=AXIS2_PLACEMENT_3D ( 'NONE', #13457, #11941, #7417 ) ;
#5686=ORIENTED_EDGE ( 'NONE', *, *, #10963, .T. ) ;
#5768=DIRECTION ( 'NONE',  ( -1.000000000000000000, 3.326610055774637112E-18, 1.062480551894331163E-17 ) ) ;
#5814=CIRCLE ( 'NONE', #15212, 2.750000000000002665 ) ;
#5857=CARTESIAN_POINT ( 'NONE',  ( 0.002394265188360167329, 0.4000000000000062395, -2.473000379418545780 ) ) ;
#5868=CARTESIAN_POINT ( 'NONE',  ( 0.2023276174660176285, 0.4000000000000061839, 2.561683098399134106 ) ) ;
#5919=CARTESIAN_POINT ( 'NONE',  ( 0.000000000000000000, 0.000000000000000000, 0.000000000000000000 ) ) ;
#5934=DIRECTION ( 'NONE',  ( -1.000000000000000000, 3.326610055774637112E-18, 1.062480551894331163E-17 ) ) ;
#5970=LINE ( 'NONE', #5090, #13557 ) ;
#6096=DIRECTION ( 'NONE',  ( 1.062480551894329468E-17, 3.608224830031754812E-16, -1.000000000000000000 ) ) ;
#6135=EDGE_CURVE ( 'NONE', #6640, #13830, #12490, .T. ) ;
#6164=ORIENTED_EDGE ( 'NONE', *, *, #14946, .T. ) ;
#6268=CARTESIAN_POINT ( 'NONE',  ( 7.000000000000006217, 5.005650134388747156E-16, -1.500000000000000000 ) ) ;
#6298=VERTEX_POINT ( 'NONE', #6268 ) ;
#6346=PRODUCT_DEFINITION ( 'UNKNOWN', '', #2733, #526 ) ;
#6403=ORIENTED_EDGE ( 'NONE', *, *, #2065, .T. ) ;
#6450=CARTESIAN_POINT ( 'NONE',  ( 0.09128442572522987852, 0.4000000000000062395, -2.551849451881606168 ) ) ;
#6451=SURFACE_SIDE_STYLE ('',( #1728 ) ) ;
#6455=CARTESIAN_POINT ( 'NONE',  ( 0.07473532696167239919, -0.3999999999999941380, -2.548950835425553674 ) ) ;
#6511=CIRCLE ( 'NONE', #2152, 2.649388036945190095 ) ;
#6546=CARTESIAN_POINT ( 'NONE',  ( 7.000000000000006217, 0.000000000000000000, 0.000000000000000000 ) ) ;
#6585=DIRECTION ( 'NONE',  ( -1.062480551894329468E-17, -3.608224830031754812E-16, 1.000000000000000000 ) ) ;
#6640=VERTEX_POINT ( 'NONE', #8645 ) ;
#6646=DIRECTION ( 'NONE',  ( 1.062480551894331009E-17, -2.775557561562888393E-16, 1.000000000000000000 ) ) ;
#6680=CARTESIAN_POINT ( 'NONE',  ( 0.000000000000000000, 0.000000000000000000, 0.000000000000000000 ) ) ;
#6707=AXIS2_PLACEMENT_3D ( 'NONE', #9555, #13284, #7479 ) ;
#6730=EDGE_LOOP ( 'NONE', ( #7116, #82 ) ) ;
#6743=CARTESIAN_POINT ( 'NONE',  ( 0.07711543383008488683, 0.4000000000000062395, -2.550194499910687362 ) ) ;
#6755=CIRCLE ( 'NONE', #15642, 1.500000000000001776 ) ;
#6765=CARTESIAN_POINT ( 'NONE',  ( 0.02995359663100405703, 0.4000000000000062395, 2.524107975521145963 ) ) ;
#6766=CARTESIAN_POINT ( 'NONE',  ( 0.09999999999998898659, 0.000000000000000000, 0.000000000000000000 ) ) ;
#6785=EDGE_CURVE ( 'NONE', #6298, #13541, #8198, .T. ) ;
#6820=CONICAL_SURFACE ( 'NONE', #9610, 2.575022672948154234, 0.08726646259971664044 ) ;
#6830=DIRECTION ( 'NONE',  ( 1.000000000000000000, -3.326610055774643275E-18, 1.062480551894329622E-17 ) ) ;
#6835=CARTESIAN_POINT ( 'NONE',  ( 0.4244143561419055910, 0.4000000000000062395, 2.581346380257589779 ) ) ;
#6845=CARTESIAN_POINT ( 'NONE',  ( 5.039986462824843482E-06, 0.4000000000000080158, 2.452138453183382971 ) ) ;
#6922=CARTESIAN_POINT ( 'NONE',  ( 0.08707474757428863843, 0.4000000000000061839, 2.551476655618785561 ) ) ;
#6974=CARTESIAN_POINT ( 'NONE',  ( 0.004861884284635707709, 0.4000000000000062395, -2.484217348758675392 ) ) ;
#6986=DIRECTION ( 'NONE',  ( -1.062480551894329930E-17, -2.775557561562888393E-16, 1.000000000000000000 ) ) ;
#7003=FACE_OUTER_BOUND ( 'NONE', #11952, .T. ) ;
#7039=VERTEX_POINT ( 'NONE', #441 ) ;
#7049=CARTESIAN_POINT ( 'NONE',  ( 0.08820272154344555027, 0.4000000000000062395, -2.551527784092946227 ) ) ;
#7076=DIRECTION ( 'NONE',  ( 1.000000000000000000, -3.326610055774637112E-18, -1.062480551894331163E-17 ) ) ;
#7082=DIRECTION ( 'NONE',  ( 0.9961946980917455452, -1.683102924354769481E-17, 0.08715574274765841567 ) ) ;
#7104=CYLINDRICAL_SURFACE ( 'NONE', #5653, 1.500000000000001776 ) ;
#7116=ORIENTED_EDGE ( 'NONE', *, *, #6135, .T. ) ;
#7138=ORIENTED_EDGE ( 'NONE', *, *, #267, .T. ) ;
#7224=CARTESIAN_POINT ( 'NONE',  ( 0.05965787728184901439, -0.3999999999999923617, 2.543631975746904139 ) ) ;
#7300=CARTESIAN_POINT ( 'NONE',  ( 0.000000000000000000, -0.3999999999999941380, 2.450963827680237017 ) ) ;
#7329=AXIS2_PLACEMENT_3D ( 'NONE', #10786, #14353, #14685 ) ;
#7417=DIRECTION ( 'NONE',  ( 0.000000000000000000, -2.775557561562887900E-16, 1.000000000000000000 ) ) ;
#7420=DIRECTION ( 'NONE',  ( -1.000000000000000000, 3.326610055774637112E-18, 1.062480551894331163E-17 ) ) ;
#7453=ADVANCED_FACE ( 'NONE', ( #13531 ), #7104, .T. ) ;
#7479=DIRECTION ( 'NONE',  ( -1.062480551894329776E-17, -2.775557561562888393E-16, 1.000000000000000000 ) ) ;
#7508=CLOSED_SHELL ( 'NONE', ( #2010, #7453, #4088, #8191, #15430, #13657, #5128, #13129, #13661, #9712, #8829, #8048, #12730 ) ) ;
#7533=DIRECTION ( 'NONE',  ( -1.000000000000000000, 3.326610055774637112E-18, 1.062480551894331163E-17 ) ) ;
#7584=ORIENTED_EDGE ( 'NONE', *, *, #6785, .T. ) ;
#7589=CARTESIAN_POINT ( 'NONE',  ( 0.4244143561419055910, -0.3999999999999906408, -2.581346380257606654 ) ) ;
#7656=ADVANCED_BREP_SHAPE_REPRESENTATION ( '', ( #15721, #14201 ), #3292 ) ;
#7663=FACE_OUTER_BOUND ( 'NONE', #2732, .T. ) ;
#7677=ORIENTED_EDGE ( 'NONE', *, *, #7740, .F. ) ;
#7687=( NAMED_UNIT ( * ) SI_UNIT ( $, .STERADIAN. ) SOLID_ANGLE_UNIT ( ) );
#7706=CARTESIAN_POINT ( 'NONE',  ( 0.02899383802118515874, -0.3999999999999941380, -2.522283165497671842 ) ) ;
#7740=EDGE_CURVE ( 'NONE', #7039, #7931, #1319, .T. ) ;
#7867=CARTESIAN_POINT ( 'NONE',  ( 0.2023276174663752591, 0.4000000000000047962, -2.561683098399166081 ) ) ;
#7873=CARTESIAN_POINT ( 'NONE',  ( 0.01582671320853740182, 0.4000000000000062395, 2.506804715526693261 ) ) ;
#7893=ORIENTED_EDGE ( 'NONE', *, *, #10036, .T. ) ;
#7931=VERTEX_POINT ( 'NONE', #8162 ) ;
#7953=AXIS2_PLACEMENT_3D ( 'NONE', #12998, #5934, #909 ) ;
#7980=EDGE_CURVE ( 'NONE', #13830, #6640, #8982, .T. ) ;
#8026=CARTESIAN_POINT ( 'NONE',  ( 0.0002101186055506396033, 0.4000000000000080158, 2.464086358652667563 ) ) ;
#8039=CARTESIAN_POINT ( 'NONE',  ( 0.000000000000000000, 0.4000000000000062395, 2.749999999999994227 ) ) ;
#8048=ADVANCED_FACE ( 'NONE', ( #15723 ), #13320, .F. ) ;
#8086=CARTESIAN_POINT ( 'NONE',  ( 0.04609070931574436175, 0.4000000000000045186, -2.537007826417986944 ) ) ;
#8108=AXIS2_PLACEMENT_3D ( 'NONE', #12587, #8793, #342 ) ;
#8110=CARTESIAN_POINT ( 'NONE',  ( 0.03853763818359707410, 0.4000000000000045186, 2.531640047765513213 ) ) ;
#8162=CARTESIAN_POINT ( 'NONE',  ( 0.000000000000000000, -0.3999999999999941380, 2.450963827680237017 ) ) ;
#8189=AXIS2_PLACEMENT_3D ( 'NONE', #9692, #9611, #14531 ) ;
#8191=ADVANCED_FACE ( 'NONE', ( #2898 ), #14821, .T. ) ;
#8198=CIRCLE ( 'NONE', #3103, 1.500000000000001776 ) ;
#8200=DIRECTION ( 'NONE',  ( 1.062480551894329776E-17, 2.775557561562888393E-16, -1.000000000000000000 ) ) ;
#8276=PLANE ( 'NONE',  #1498 ) ;
#8279=EDGE_CURVE ( 'NONE', #6298, #13830, #15540, .T. ) ;
#8393=DIRECTION ( 'NONE',  ( -1.000000000000000000, 3.326610055774637112E-18, 1.062480551894331163E-17 ) ) ;
#8398=ORIENTED_EDGE ( 'NONE', *, *, #70, .T. ) ;
#8420=CARTESIAN_POINT ( 'NONE',  ( 0.0002870078139504136732, -0.3999999999999958589, 2.459819222911289405 ) ) ;
#8456=EDGE_CURVE ( 'NONE', #3287, #14081, #321, .T. ) ;
#8504=CARTESIAN_POINT ( 'NONE',  ( 0.0008577403172727038339, -0.3999999999999958589, 2.464205331206099192 ) ) ;
#8531=PLANE ( 'NONE',  #6707 ) ;
#8543=AXIS2_PLACEMENT_3D ( 'NONE', #15254, #3081, #6986 ) ;
#8645=CARTESIAN_POINT ( 'NONE',  ( 2.000000000000001776, -4.163336342344337027E-16, 1.500000000000001776 ) ) ;
#8748=VERTEX_POINT ( 'NONE', #9017 ) ;
#8768=VECTOR ( 'NONE', #12067, 1000.000000000000000 ) ;
#8785=ORIENTED_EDGE ( 'NONE', *, *, #1894, .F. ) ;
#8793=DIRECTION ( 'NONE',  ( -1.000000000000000000, 3.326610055774637112E-18, 1.062480551894331163E-17 ) ) ;
#8796=CARTESIAN_POINT ( 'NONE',  ( 0.09128442574521389297, -0.3999999999999975797, -2.551849451998178253 ) ) ;
#8829=ADVANCED_FACE ( 'NONE', ( #5586 ), #8531, .F. ) ;
#8877=CARTESIAN_POINT ( 'NONE',  ( 0.5662760513513173111, -0.3999999999999906408, -2.593905796088002091 ) ) ;
#8879=CARTESIAN_POINT ( 'NONE',  ( 0.09128442574521389297, -0.3999999999999975797, -2.551849451998178253 ) ) ;
#8898=( NAMED_UNIT ( * ) PLANE_ANGLE_UNIT ( ) SI_UNIT ( $, .RADIAN. ) );
#8925=CARTESIAN_POINT ( 'NONE',  ( 0.09128442572436945568, 0.4000000000000010214, 2.551849451885215725 ) ) ;
#8947=DIRECTION ( 'NONE',  ( 0.000000000000000000, -2.775557561562887900E-16, 1.000000000000000000 ) ) ;
#8982=CIRCLE ( 'NONE', #7953, 1.500000000000001776 ) ;
#8995=( NAMED_UNIT ( * ) SI_UNIT ( $, .STERADIAN. ) SOLID_ANGLE_UNIT ( ) );
#9017=CARTESIAN_POINT ( 'NONE',  ( 0.000000000000000000, 0.4000000000000062395, -2.450963827680254337 ) ) ;
#9067=ORIENTED_EDGE ( 'NONE', *, *, #3958, .T. ) ;
#9075=CARTESIAN_POINT ( 'NONE',  ( 0.01439699119390668372, -0.3999999999999975797, -2.504551029406990370 ) ) ;
#9080=CARTESIAN_POINT ( 'NONE',  ( -1.105332846508322361E-14, 0.4000000000000061284, 2.451551129619757408 ) ) ;
#9103=ORIENTED_EDGE ( 'NONE', *, *, #1035, .T. ) ;
#9117=AXIS2_PLACEMENT_3D ( 'NONE', #4608, #7076, #13651 ) ;
#9211=VECTOR ( 'NONE', #6585, 1000.000000000000000 ) ;
#9221=AXIS2_PLACEMENT_3D ( 'NONE', #13460, #7420, #4880 ) ;
#9249=ORIENTED_EDGE ( 'NONE', *, *, #8279, .T. ) ;
#9252=ORIENTED_EDGE ( 'NONE', *, *, #10963, .F. ) ;
#9288=DIRECTION ( 'NONE',  ( -1.062480551894329776E-17, -2.775557561562888393E-16, 1.000000000000000000 ) ) ;
#9331=AXIS2_PLACEMENT_3D ( 'NONE', #1561, #7533, #1398 ) ;
#9354=CARTESIAN_POINT ( 'NONE',  ( 0.09128442572522987852, 0.4000000000000062395, -2.551849451881606168 ) ) ;
#9397=ORIENTED_EDGE ( 'NONE', *, *, #12918, .T. ) ;
#9405=EDGE_CURVE ( 'NONE', #14984, #11235, #11366, .T. ) ;
#9555=CARTESIAN_POINT ( 'NONE',  ( 0.8499999999999896527, 0.4000000000000062395, 2.749999999999994227 ) ) ;
#9559=ORIENTED_EDGE ( 'NONE', *, *, #12454, .T. ) ;
#9560=EDGE_LOOP ( 'NONE', ( #1745, #9252, #11828, #14417, #4870, #4810 ) ) ;
#9610=AXIS2_PLACEMENT_3D ( 'NONE', #10110, #11372, #3173 ) ;
#9611=DIRECTION ( 'NONE',  ( -1.000000000000000000, 3.326610055774637112E-18, 1.062480551894331163E-17 ) ) ;
#9631=FACE_OUTER_BOUND ( 'NONE', #15532, .T. ) ;
#9634=VECTOR ( 'NONE', #15631, 1000.000000000000000 ) ;
#9673=UNCERTAINTY_MEASURE_WITH_UNIT (LENGTH_MEASURE( 1.000000000000000082E-05 ), #2841, 'distance_accuracy_value', 'NONE');
#9689=CARTESIAN_POINT ( 'NONE',  ( 0.02317000962515113754, -0.3999999999999923617, 2.516813694799619139 ) ) ;
#9692=CARTESIAN_POINT ( 'NONE',  ( 2.000000000000001776, 0.000000000000000000, 0.000000000000000000 ) ) ;
#9712=ADVANCED_FACE ( 'NONE', ( #10646 ), #15090, .T. ) ;
#9879=VERTEX_POINT ( 'NONE', #2999 ) ;
#10006=SURFACE_SIDE_STYLE ('',( #2759 ) ) ;
#10024=CARTESIAN_POINT ( 'NONE',  ( -1.294371610423890733E-14, -0.3999999999999905853, -2.454447735324990276 ) ) ;
#10036=EDGE_CURVE ( 'NONE', #14984, #15527, #11926, .T. ) ;
#10110=CARTESIAN_POINT ( 'NONE',  ( 0.000000000000000000, 0.000000000000000000, 0.000000000000000000 ) ) ;
#10178=CARTESIAN_POINT ( 'NONE',  ( 0.001687421788282983956, -0.3999999999999906408, -2.472702538403935169 ) ) ;
#10267=ORIENTED_EDGE ( 'NONE', *, *, #10776, .T. ) ;
#10280=EDGE_CURVE ( 'NONE', #1532, #1004, #5970, .T. ) ;
#10313=FILL_AREA_STYLE ('',( #5234 ) ) ;
#10330=( NAMED_UNIT ( * ) PLANE_ANGLE_UNIT ( ) SI_UNIT ( $, .RADIAN. ) );
#10356=CONICAL_SURFACE ( 'NONE', #10613, 2.575022672948154234, 0.08726646259971664044 ) ;
#10371=B_SPLINE_CURVE_WITH_KNOTS ( 'NONE', 3,
 ( #11816, #12775, #1879, #6835, #1006, #5868, #10716 ),
 .UNSPECIFIED., .F., .F.,
 ( 4, 3, 4 ),
 ( 0.004378233155234298977, 0.004805482862474828344, 0.005139916140553234432 ),
 .UNSPECIFIED. ) ;
#10373=SHAPE_DEFINITION_REPRESENTATION ( #14518, #4596 ) ;
#10395=CARTESIAN_POINT ( 'NONE',  ( 0.01925117833309565596, 0.4000000000000027978, -2.511168856671952554 ) ) ;
#10416=CARTESIAN_POINT ( 'NONE',  ( 0.006257361140793449295, 0.4000000000000027978, 2.486236325722958718 ) ) ;
#10457=ORIENTED_EDGE ( 'NONE', *, *, #12454, .F. ) ;
#10499=ORIENTED_EDGE ( 'NONE', *, *, #2916, .F. ) ;
#10567=CARTESIAN_POINT ( 'NONE',  ( 0.08288047105113569013, 0.4000000000000045186, 2.550831915580193510 ) ) ;
#10588=ORIENTED_EDGE ( 'NONE', *, *, #10280, .T. ) ;
#10602=CARTESIAN_POINT ( 'NONE',  ( -25.39999999999994884, 6.000306541065368193E-16, -1.500000000000001776 ) ) ;
#10613=AXIS2_PLACEMENT_3D ( 'NONE', #1258, #3805, #13276 ) ;
#10633=FACE_OUTER_BOUND ( 'NONE', #3817, .T. ) ;
#10646=FACE_OUTER_BOUND ( 'NONE', #13250, .T. ) ;
#10703=CARTESIAN_POINT ( 'NONE',  ( 0.02384593234141434148, 0.4000000000000097367, -2.517027090855607607 ) ) ;
#10710=ORIENTED_EDGE ( 'NONE', *, *, #5465, .F. ) ;
#10716=CARTESIAN_POINT ( 'NONE',  ( 0.09128442572436945568, 0.4000000000000010214, 2.551849451885215725 ) ) ;
#10747=AXIS2_PLACEMENT_3D ( 'NONE', #1148, #13552, #6096 ) ;
#10749=ORIENTED_EDGE ( 'NONE', *, *, #12609, .F. ) ;
#10774=CARTESIAN_POINT ( 'NONE',  ( -25.39999999999994884, -4.163336342344337027E-16, 1.500000000000001776 ) ) ;
#10776=EDGE_CURVE ( 'NONE', #2165, #1532, #6511, .T. ) ;
#10786=CARTESIAN_POINT ( 'NONE',  ( 0.8499999999999896527, -0.3999999999999906408, -2.750000000000010658 ) ) ;
#10871=EDGE_LOOP ( 'NONE', ( #8398, #9249, #13368, #4927 ) ) ;
#10896=LINE ( 'NONE', #12081, #3489 ) ;
#10910=ORIENTED_EDGE ( 'NONE', *, *, #15329, .T. ) ;
#10963=EDGE_CURVE ( 'NONE', #14081, #2165, #5565, .T. ) ;
#11135=AXIS2_PLACEMENT_3D ( 'NONE', #2325, #1059, #12037 ) ;
#11177=COLOUR_RGB ( '', 0.66274510, 0.83137255, 0.94901961) ;
#11235=VERTEX_POINT ( 'NONE', #2995 ) ;
#11281=CARTESIAN_POINT ( 'NONE',  ( 0.8499999999999896527, 0.4000000000000097367, -2.619018321873355593 ) ) ;
#11284=CARTESIAN_POINT ( 'NONE',  ( 0.3133709289737746650, 0.4000000000000062395, -2.571515392583464621 ) ) ;
#11287=CARTESIAN_POINT ( 'NONE',  ( 0.09128442574521389297, -0.3999999999999975797, -2.551849451998178253 ) ) ;
#11323=EDGE_CURVE ( 'NONE', #8748, #9879, #13728, .T. ) ;
#11344=( NAMED_UNIT ( * ) SI_UNIT ( $, .STERADIAN. ) SOLID_ANGLE_UNIT ( ) );
#11365=CARTESIAN_POINT ( 'NONE',  ( 2.000000000000001776, 7.566251093182458196E-16, -2.750000000000003109 ) ) ;
#11366=LINE ( 'NONE', #314, #3149 ) ;
#11371=ORIENTED_EDGE ( 'NONE', *, *, #10776, .F. ) ;
#11372=DIRECTION ( 'NONE',  ( 1.000000000000000000, -3.326610055774637112E-18, -1.062480551894331163E-17 ) ) ;
#11388=EDGE_LOOP ( 'NONE', ( #13289, #13614, #5342, #1835, #980, #10749, #10588, #11410 ) ) ;
#11410=ORIENTED_EDGE ( 'NONE', *, *, #1894, .T. ) ;
#11421=SHAPE_REPRESENTATION_RELATIONSHIP ( 'NONE' , 'NONE' ,  #4596, #7656 ) ;
#11462=B_SPLINE_CURVE_WITH_KNOTS ( 'NONE', 3,
 ( #12479, #387, #2704, #5257, #12559, #1657, #13753 ),
 .UNSPECIFIED., .F., .F.,
 ( 4, 3, 4 ),
 ( 0.004471049636503268004, 0.004805482912052319762, 0.005232732616948215093 ),
 .UNSPECIFIED. ) ;
#11513=DIRECTION ( 'NONE',  ( 0.000000000000000000, 0.000000000000000000, 1.000000000000000000 ) ) ;
#11554=DIRECTION ( 'NONE',  ( -1.000000000000000000, 3.326610055774637112E-18, 1.062480551894331163E-17 ) ) ;
#11566=CARTESIAN_POINT ( 'NONE',  ( 0.8499999999999896527, 0.4000000000000062395, 2.619018321873338273 ) ) ;
#11664=MECHANICAL_DESIGN_GEOMETRIC_PRESENTATION_REPRESENTATION('',(#2776),#4818);
#11666=DIRECTION ( 'NONE',  ( 1.062480551894329776E-17, 2.775557561562888393E-16, -1.000000000000000000 ) ) ;
#11683=DIRECTION ( 'NONE',  ( -1.000000000000000000, 3.326610055774637112E-18, 1.062480551894331163E-17 ) ) ;
#11816=CARTESIAN_POINT ( 'NONE',  ( 0.8499999999999896527, 0.4000000000000062395, 2.619018321873338273 ) ) ;
#11828=ORIENTED_EDGE ( 'NONE', *, *, #5465, .T. ) ;
#11832=CARTESIAN_POINT ( 'NONE',  ( 0.000000000000000000, 0.000000000000000000, 0.000000000000000000 ) ) ;
#11884=CARTESIAN_POINT ( 'NONE',  ( 0.09025563639527389714, 0.4000000000000047962, -2.551758345435058306 ) ) ;
#11896=CARTESIAN_POINT ( 'NONE',  ( 0.005811324839270699469, -0.3999999999999993006, 2.486892833834318139 ) ) ;
#11926=B_SPLINE_CURVE_WITH_KNOTS ( 'NONE', 3,
 ( #4083, #12742, #8877, #7589, #12437, #2894, #8796 ),
 .UNSPECIFIED., .F., .F.,
 ( 4, 3, 4 ),
 ( 0.004378233155234299845, 0.004805482862474828344, 0.005139916140522488193 ),
 .UNSPECIFIED. ) ;
#11941=DIRECTION ( 'NONE',  ( -1.000000000000000000, 3.326610055774637112E-18, 1.062480551894331163E-17 ) ) ;
#11952=EDGE_LOOP ( 'NONE', ( #7677, #9559 ) ) ;
#12037=DIRECTION ( 'NONE',  ( -1.049359643968190670E-17, -1.165734175856414170E-15, 1.000000000000000000 ) ) ;
#12061=CARTESIAN_POINT ( 'NONE',  ( 0.8499999999999896527, -0.3999999999999941380, -2.619018321873356037 ) ) ;
#12067=DIRECTION ( 'NONE',  ( 1.062480551894329776E-17, 2.775557561562888393E-16, -1.000000000000000000 ) ) ;
#12081=CARTESIAN_POINT ( 'NONE',  ( -2.735911510694367108E-17, -3.993630376939310903E-16, 2.575022672948154234 ) ) ;
#12140=CARTESIAN_POINT ( 'NONE',  ( 0.04931887323393824990, -0.3999999999999923617, 2.539017587791714714 ) ) ;
#12199=UNCERTAINTY_MEASURE_WITH_UNIT (LENGTH_MEASURE( 1.000000000000000082E-05 ), #12535, 'distance_accuracy_value', 'NONE');
#12256=ORIENTED_EDGE ( 'NONE', *, *, #3115, .F. ) ;
#12309=CARTESIAN_POINT ( 'NONE',  ( 7.000000000000006217, -4.163336342344337027E-16, 1.500000000000001776 ) ) ;
#12387=AXIS2_PLACEMENT_3D ( 'NONE', #5321, #13576, #14860 ) ;
#12437=CARTESIAN_POINT ( 'NONE',  ( 0.3133709289838055301, -0.3999999999999906408, -2.571515392584351023 ) ) ;
#12441=DIRECTION ( 'NONE',  ( -1.000000000000000000, 3.326610055774637112E-18, 1.062480551894331163E-17 ) ) ;
#12454=EDGE_CURVE ( 'NONE', #7039, #7931, #4707, .T. ) ;
#12476=DIRECTION ( 'NONE',  ( -1.000000000000000000, 3.326610055774643275E-18, -1.062480551894329622E-17 ) ) ;
#12479=CARTESIAN_POINT ( 'NONE',  ( 0.09128442572411965550, -0.3999999999999975797, 2.551849451881568420 ) ) ;
#12490=CIRCLE ( 'NONE', #8189, 1.500000000000001776 ) ;
#12535=( LENGTH_UNIT ( ) NAMED_UNIT ( * ) SI_UNIT ( .MILLI., .METRE. ) );
#12559=CARTESIAN_POINT ( 'NONE',  ( 0.5662760513513177552, -0.3999999999999975797, 2.593905796087984328 ) ) ;
#12587=CARTESIAN_POINT ( 'NONE',  ( -25.39999999999994884, 0.000000000000000000, 0.000000000000000000 ) ) ;
#12602=EDGE_CURVE ( 'NONE', #3171, #15527, #14420, .T. ) ;
#12609=EDGE_CURVE ( 'NONE', #1532, #14984, #12893, .T. ) ;
#12631=CARTESIAN_POINT ( 'NONE',  ( 0.0005321174777195292194, -0.3999999999999906408, -2.461401996259243496 ) ) ;
#12675=CARTESIAN_POINT ( 'NONE',  ( 0.09999999999998898659, 0.000000000000000000, 0.000000000000000000 ) ) ;
#12707=CARTESIAN_POINT ( 'NONE',  ( 0.5662760513513177552, 0.4000000000000062395, -2.593905796088003424 ) ) ;
#12710=CARTESIAN_POINT ( 'NONE',  ( 0.000000000000000000, -0.3999999999999958589, -2.450963827680254337 ) ) ;
#12730=ADVANCED_FACE ( 'NONE', ( #3698 ), #3382, .F. ) ;
#12742=CARTESIAN_POINT ( 'NONE',  ( 0.7081379353438689295, -0.3999999999999906408, -2.606463079733445376 ) ) ;
#12744=DIRECTION ( 'NONE',  ( 0.000000000000000000, -1.570965579844596505E-14, -1.000000000000000000 ) ) ;
#12775=CARTESIAN_POINT ( 'NONE',  ( 0.7081379353438682633, 0.4000000000000061839, 2.606463079733442711 ) ) ;
#12788=ORIENTED_EDGE ( 'NONE', *, *, #14946, .F. ) ;
#12852=PLANE ( 'NONE',  #3498 ) ;
#12893=CIRCLE ( 'NONE', #12387, 2.649388036945190095 ) ;
#12911=ORIENTED_EDGE ( 'NONE', *, *, #14182, .T. ) ;
#12918=EDGE_CURVE ( 'NONE', #9879, #13047, #14941, .T. ) ;
#12998=CARTESIAN_POINT ( 'NONE',  ( 2.000000000000001776, 0.000000000000000000, 0.000000000000000000 ) ) ;
#13019=AXIS2_PLACEMENT_3D ( 'NONE', #12675, #12441, #6646 ) ;
#13047=VERTEX_POINT ( 'NONE', #8925 ) ;
#13110=DIRECTION ( 'NONE',  ( -1.062480551894329776E-17, -2.775557561562888393E-16, 1.000000000000000000 ) ) ;
#13129=ADVANCED_FACE ( 'NONE', ( #5263 ), #6820, .T. ) ;
#13213=STYLED_ITEM ( 'NONE', ( #521 ), #7656 ) ;
#13229=DIRECTION ( 'NONE',  ( -1.062480551894329930E-17, -2.775557561562888393E-16, 1.000000000000000000 ) ) ;
#13250=EDGE_LOOP ( 'NONE', ( #2192, #4689, #12788, #10457 ) ) ;
#13256=CARTESIAN_POINT ( 'NONE',  ( 0.01615993435121231697, -0.3999999999999993006, 2.507354378531367889 ) ) ;
#13276=DIRECTION ( 'NONE',  ( 1.062480551894329776E-17, 2.775557561562888393E-16, -1.000000000000000000 ) ) ;
#13284=DIRECTION ( 'NONE',  ( -3.326610055774640964E-18, 1.000000000000000000, 2.775557561562888393E-16 ) ) ;
#13289=ORIENTED_EDGE ( 'NONE', *, *, #2065, .F. ) ;
#13292=EDGE_LOOP ( 'NONE', ( #2714, #876, #1582, #2068 ) ) ;
#13320=PLANE ( 'NONE',  #10747 ) ;
#13368=ORIENTED_EDGE ( 'NONE', *, *, #6135, .F. ) ;
#13457=CARTESIAN_POINT ( 'NONE',  ( -25.39999999999994884, 0.000000000000000000, 0.000000000000000000 ) ) ;
#13460=CARTESIAN_POINT ( 'NONE',  ( 0.8499999999999896527, 0.000000000000000000, 0.000000000000000000 ) ) ;
#13531=FACE_OUTER_BOUND ( 'NONE', #10871, .T. ) ;
#13541=VERTEX_POINT ( 'NONE', #12309 ) ;
#13552=DIRECTION ( 'NONE',  ( 3.326610055774640194E-18, -1.000000000000000000, -3.608224830031754812E-16 ) ) ;
#13557=VECTOR ( 'NONE', #1412, 1000.000000000000000 ) ;
#13576=DIRECTION ( 'NONE',  ( -1.000000000000000000, 3.326610055774637112E-18, 1.062480551894331163E-17 ) ) ;
#13582=AXIS2_PLACEMENT_3D ( 'NONE', #5919, #8393, #13229 ) ;
#13614=ORIENTED_EDGE ( 'NONE', *, *, #14182, .F. ) ;
#13634=ORIENTED_EDGE ( 'NONE', *, *, #7980, .F. ) ;
#13651=DIRECTION ( 'NONE',  ( -1.049359643968190670E-17, -2.775557561562888393E-16, 1.000000000000000000 ) ) ;
#13657=ADVANCED_FACE ( 'NONE', ( #607 ), #12852, .T. ) ;
#13661=ADVANCED_FACE ( 'NONE', ( #10633, #5479 ), #4273, .F. ) ;
#13666=PLANE ( 'NONE',  #4530 ) ;
#13701=ORIENTED_EDGE ( 'NONE', *, *, #7740, .T. ) ;
#13728=B_SPLINE_CURVE_WITH_KNOTS ( 'NONE', 3,
 ( #15488, #835, #5547, #5857, #6974, #2024, #910, #10395, #10703, #1869, #2178, #8086, #3150, #4266, #6743, #7049, #14195, #11884, #9354 ),
 .UNSPECIFIED., .F., .F.,
 ( 4, 3, 3, 3, 3, 3, 4 ),
 ( 0.0005509418849372115044, 0.0005730732227554590505, 0.0006075432786058860765, 0.0006294361076369635061, 0.0006629275523618718491, 0.0006964354412241015486, 0.0006994975975014303734 ),
 .UNSPECIFIED. ) ;
#13753=CARTESIAN_POINT ( 'NONE',  ( 0.8499999999999896527, -0.3999999999999958589, 2.619018321873339161 ) ) ;
#13824=CARTESIAN_POINT ( 'NONE',  ( 0.04451878633413008934, -0.3999999999999923617, -2.535225719870653815 ) ) ;
#13830=VERTEX_POINT ( 'NONE', #4911 ) ;
#13881=SURFACE_STYLE_USAGE ( .BOTH. , #10006 ) ;
#13917=AXIS2_PLACEMENT_3D ( 'NONE', #767, #15334, #9288 ) ;
#13929=AXIS2_PLACEMENT_3D ( 'NONE', #899, #5768, #3365 ) ;
#13987=CARTESIAN_POINT ( 'NONE',  ( 0.02292651764862485564, 0.4000000000000062395, 2.515500884275507776 ) ) ;
#13999=EDGE_CURVE ( 'NONE', #3420, #1004, #5814, .T. ) ;
#14061=CARTESIAN_POINT ( 'NONE',  ( 0.002345414276150574722, 0.4000000000000027978, 2.475568618642806307 ) ) ;
#14081=VERTEX_POINT ( 'NONE', #11566 ) ;
#14147=CIRCLE ( 'NONE', #9331, 2.750000000000002665 ) ;
#14182=EDGE_CURVE ( 'NONE', #11235, #3287, #3254, .T. ) ;
#14195=CARTESIAN_POINT ( 'NONE',  ( 0.08922814936599068880, 0.4000000000000062395, -2.551651095287820414 ) ) ;
#14201=AXIS2_PLACEMENT_3D ( 'NONE', #6680, #11513, #1651 ) ;
#14341=EDGE_LOOP ( 'NONE', ( #7893, #9067, #13701, #6164, #9103, #609 ) ) ;
#14353=DIRECTION ( 'NONE',  ( 1.000000000000000000, -3.326610055774643275E-18, 1.062480551894329622E-17 ) ) ;
#14359=CARTESIAN_POINT ( 'NONE',  ( 0.08043465938667249127, -0.3999999999999898637, 2.550888629652776185 ) ) ;
#14417=ORIENTED_EDGE ( 'NONE', *, *, #1139, .T. ) ;
#14420=CIRCLE ( 'NONE', #9117, 2.583009025355586186 ) ;
#14447=CARTESIAN_POINT ( 'NONE',  ( 0.03145189498340861256, -0.3999999999999923617, 2.524708160309380389 ) ) ;
#14485=MECHANICAL_DESIGN_GEOMETRIC_PRESENTATION_REPRESENTATION('',(#13213),#4573);
#14518=PRODUCT_DEFINITION_SHAPE ( 'NONE', 'NONE',  #6346 ) ;
#14531=DIRECTION ( 'NONE',  ( 0.000000000000000000, -2.775557561562887900E-16, 1.000000000000000000 ) ) ;
#14595=UNCERTAINTY_MEASURE_WITH_UNIT (LENGTH_MEASURE( 1.000000000000000082E-05 ), #4204, 'distance_accuracy_value', 'NONE');
#14606=CARTESIAN_POINT ( 'NONE',  ( 0.8499999999999896527, 7.325252813983392336E-16, -2.649388036945189207 ) ) ;
#14685=DIRECTION ( 'NONE',  ( 1.062480551894329776E-17, 2.775557561562888393E-16, -1.000000000000000000 ) ) ;
#14808=ORIENTED_EDGE ( 'NONE', *, *, #8456, .F. ) ;
#14821=TOROIDAL_SURFACE ( 'NONE', #13019, 2.483389555546409166, 0.1000000000000000056 ) ;
#14845=CARTESIAN_POINT ( 'NONE',  ( 2.000000000000001776, 0.000000000000000000, 0.000000000000000000 ) ) ;
#14860=DIRECTION ( 'NONE',  ( 0.000000000000000000, 2.775557561562887900E-16, -1.000000000000000000 ) ) ;
#14872=CARTESIAN_POINT ( 'NONE',  ( 0.08570591359081922156, -0.3999999999999906408, -2.551355435856202281 ) ) ;
#14941=CIRCLE ( 'NONE', #11135, 2.583009025355586186 ) ;
#14946=EDGE_CURVE ( 'NONE', #7931, #3171, #5214, .T. ) ;
#14953=CARTESIAN_POINT ( 'NONE',  ( 0.08014973387278834238, -0.3999999999999941380, -2.550381935564455027 ) ) ;
#14984=VERTEX_POINT ( 'NONE', #12061 ) ;
#14985=CARTESIAN_POINT ( 'NONE',  ( 7.000000000000006217, 0.000000000000000000, 0.000000000000000000 ) ) ;
#15031=CARTESIAN_POINT ( 'NONE',  ( 0.03893478199943582047, -0.3999999999999923617, -2.531455901217069204 ) ) ;
#15090=TOROIDAL_SURFACE ( 'NONE', #5443, 2.483389555546409166, 0.1000000000000000056 ) ;
#15106=FILL_AREA_STYLE ('',( #4122 ) ) ;
#15112=CARTESIAN_POINT ( 'NONE',  ( 0.09128442572436945568, 0.4000000000000010214, 2.551849451885215725 ) ) ;
#15148=CARTESIAN_POINT ( 'NONE',  ( 0.8499999999999896527, 0.000000000000000000, 0.000000000000000000 ) ) ;
#15212=AXIS2_PLACEMENT_3D ( 'NONE', #14845, #4174, #3211 ) ;
#15254=CARTESIAN_POINT ( 'NONE',  ( 0.000000000000000000, 0.000000000000000000, 0.000000000000000000 ) ) ;
#15257=CARTESIAN_POINT ( 'NONE',  ( 0.09128442572411965550, -0.3999999999999975797, 2.551849451881568420 ) ) ;
#15259=SURFACE_STYLE_USAGE ( .BOTH. , #6451 ) ;
#15279=LINE ( 'NONE', #8039, #3739 ) ;
#15329=EDGE_CURVE ( 'NONE', #13541, #6640, #3368, .T. ) ;
#15331=APPLICATION_CONTEXT ( 'automotive_design' ) ;
#15334=DIRECTION ( 'NONE',  ( -1.000000000000000000, 3.326610055774643275E-18, -1.062480551894329622E-17 ) ) ;
#15430=ADVANCED_FACE ( 'NONE', ( #7663 ), #499, .T. ) ;
#15488=CARTESIAN_POINT ( 'NONE',  ( 0.000000000000000000, 0.4000000000000062395, -2.450963827680254337 ) ) ;
#15527=VERTEX_POINT ( 'NONE', #8879 ) ;
#15528=ORIENTED_EDGE ( 'NONE', *, *, #6785, .F. ) ;
#15532=EDGE_LOOP ( 'NONE', ( #14808, #6403, #4576, #723, #11371, #12256, #9397, #10710 ) ) ;
#15540=LINE ( 'NONE', #10602, #4393 ) ;
#15631=DIRECTION ( 'NONE',  ( -1.000000000000000000, 3.326610055774637112E-18, 1.062480551894331163E-17 ) ) ;
#15642=AXIS2_PLACEMENT_3D ( 'NONE', #14985, #4076, #8947 ) ;
#15721=MANIFOLD_SOLID_BREP ( 'Slot', #7508 ) ;
#15723=FACE_OUTER_BOUND ( 'NONE', #14341, .T. ) ;
ENDSEC;
END-ISO-10303-21;
